ISO-10303-21;
HEADER;
FILE_DESCRIPTION (('STEP AP214'),
    '1' );
FILE_NAME ('roller axis assy_r6.step',
    '2026-10-24T11:01:53',
    ( '' ),
    ( '' ),
    'SwSTEP 2.0',
    'SolidWorks 2026',
    '' );
FILE_SCHEMA (( 'AUTOMOTIVE_DESIGN' ));
ENDSEC;

DATA;
#10=LINE ( 'NONE', #1868, #5341 ) ;
#37=AXIS2_PLACEMENT_3D ( 'NONE', #3813, #3117, #8346 ) ;
#49=CARTESIAN_POINT ( 'NONE',  ( 20.00000000000000000, 0.000000000000000000, 120.0000000000000142 ) ) ;
#88=EDGE_CURVE ( 'NONE', #3290, #1917, #5360, .T. ) ;
#89=DIRECTION ( 'NONE',  ( -1.000000000000000000, 0.000000000000000000, -0.000000000000000000 ) ) ;
#94=ORIENTED_EDGE ( 'NONE', *, *, #7928, .T. ) ;
#97=CARTESIAN_POINT ( 'NONE',  ( 10.00000000000000000, 0.000000000000000000, 42.00000000000000711 ) ) ;
#115=( LENGTH_UNIT ( ) NAMED_UNIT ( * ) SI_UNIT ( .MILLI., .METRE. ) );
#127=DIRECTION ( 'NONE',  ( 0.000000000000000000, 0.000000000000000000, 1.000000000000000000 ) ) ;
#128=CARTESIAN_POINT ( 'NONE',  ( 5.000000000000000000, -5.000000000000000000, 34.00000000000000711 ) ) ;
#129=FACE_OUTER_BOUND ( 'NONE', #369, .T. ) ;
#139=ORIENTED_EDGE ( 'NONE', *, *, #5913, .F. ) ;
#153=PRODUCT_DEFINITION_SHAPE ( 'NONE', 'NONE',  #1825 ) ;
#155=ORIENTED_EDGE ( 'NONE', *, *, #8498, .T. ) ;
#158=CARTESIAN_POINT ( 'NONE',  ( -5.000000000000001776, 5.000000000000001776, 34.00000000000000711 ) ) ;
#178=DIRECTION ( 'NONE',  ( -0.000000000000000000, -0.000000000000000000, 1.000000000000000000 ) ) ;
#185=ORIENTED_EDGE ( 'NONE', *, *, #253, .T. ) ;
#187=CARTESIAN_POINT ( 'NONE',  ( -10.00000000000000000, 1.224646799147353256E-15, 42.00000000000000711 ) ) ;
#198=CARTESIAN_POINT ( 'NONE',  ( -10.00000000000000000, 1.224646799147353256E-15, 120.0000000000000142 ) ) ;
#206=SURFACE_SIDE_STYLE ('',( #4174 ) ) ;
#227=AXIS2_PLACEMENT_3D ( 'NONE', #2062, #2145, #1353 ) ;
#240=DIRECTION ( 'NONE',  ( -0.000000000000000000, -0.000000000000000000, 1.000000000000000000 ) ) ;
#253=EDGE_CURVE ( 'NONE', #1917, #3290, #7040, .T. ) ;
#272=ORIENTED_EDGE ( 'NONE', *, *, #334, .T. ) ;
#325=EDGE_LOOP ( 'NONE', ( #5530, #4700, #8320, #94 ) ) ;
#334=EDGE_CURVE ( 'NONE', #2939, #4339, #7033, .T. ) ;
#335=CARTESIAN_POINT ( 'NONE',  ( 5.000000000000000000, -5.000000000000000000, 140.0000000000000000 ) ) ;
#365=DIRECTION ( 'NONE',  ( -1.000000000000000000, 0.000000000000000000, 0.000000000000000000 ) ) ;
#366=CARTESIAN_POINT ( 'NONE',  ( 5.000000000000000000, -5.000000000000000000, 42.00000000000000711 ) ) ;
#369=EDGE_LOOP ( 'NONE', ( #8179, #7657, #2904, #5025 ) ) ;
#381=DIRECTION ( 'NONE',  ( 1.734723475976806848E-16, -1.000000000000000000, -0.000000000000000000 ) ) ;
#410=CARTESIAN_POINT ( 'NONE',  ( 10.00000000000000000, 0.000000000000000000, 42.00000000000000711 ) ) ;
#444=FACE_OUTER_BOUND ( 'NONE', #8384, .T. ) ;
#464=DIRECTION ( 'NONE',  ( 0.000000000000000000, 0.000000000000000000, 1.000000000000000000 ) ) ;
#478=VERTEX_POINT ( 'NONE', #1205 ) ;
#507=DIRECTION ( 'NONE',  ( 1.734723475976806848E-16, -1.000000000000000000, -0.000000000000000000 ) ) ;
#509=CARTESIAN_POINT ( 'NONE',  ( 0.000000000000000000, 0.000000000000000000, 148.0000000000000284 ) ) ;
#544=ORIENTED_EDGE ( 'NONE', *, *, #5815, .F. ) ;
#567=ADVANCED_FACE ( 'NONE', ( #8467, #3192 ), #5186, .T. ) ;
#585=ORIENTED_EDGE ( 'NONE', *, *, #6271, .T. ) ;
#594=AXIS2_PLACEMENT_3D ( 'NONE', #3123, #464, #5764 ) ;
#608=AXIS2_PLACEMENT_3D ( 'NONE', #7647, #6285, #365 ) ;
#628=VERTEX_POINT ( 'NONE', #4013 ) ;
#643=ADVANCED_FACE ( 'NONE', ( #2664 ), #5353, .F. ) ;
#685=DIRECTION ( 'NONE',  ( -1.000000000000000000, 0.000000000000000000, 0.000000000000000000 ) ) ;
#687=AXIS2_PLACEMENT_3D ( 'NONE', #1011, #5618, #4883 ) ;
#689=EDGE_LOOP ( 'NONE', ( #272, #8189, #1322, #1809 ) ) ;
#690=ORIENTED_EDGE ( 'NONE', *, *, #334, .F. ) ;
#710=ADVANCED_FACE ( 'NONE', ( #8116, #1310 ), #8590, .F. ) ;
#719=PRODUCT_DEFINITION_FORMATION_WITH_SPECIFIED_SOURCE ( 'ANY', '', #7464, .NOT_KNOWN. ) ;
#724=AXIS2_PLACEMENT_3D ( 'NONE', #6139, #2104, #89 ) ;
#755=CARTESIAN_POINT ( 'NONE',  ( -5.000000000000000000, -5.000000000000000000, 42.00000000000000711 ) ) ;
#756=AXIS2_PLACEMENT_3D ( 'NONE', #8216, #4153, #2726 ) ;
#779=ORIENTED_EDGE ( 'NONE', *, *, #3163, .F. ) ;
#788=SURFACE_STYLE_USAGE ( .BOTH. , #206 ) ;
#792=DIRECTION ( 'NONE',  ( 1.000000000000000000, 0.000000000000000000, 0.000000000000000000 ) ) ;
#833=FACE_OUTER_BOUND ( 'NONE', #5763, .T. ) ;
#852=PLANE ( 'NONE',  #6865 ) ;
#856=FACE_OUTER_BOUND ( 'NONE', #7874, .T. ) ;
#865=AXIS2_PLACEMENT_3D ( 'NONE', #8225, #5756, #7156 ) ;
#887=( GEOMETRIC_REPRESENTATION_CONTEXT ( 3 ) GLOBAL_UNCERTAINTY_ASSIGNED_CONTEXT ( ( #2680 ) ) GLOBAL_UNIT_ASSIGNED_CONTEXT ( ( #7558, #8174, #943 ) ) REPRESENTATION_CONTEXT ( 'NONE', 'WORKASPACE' ) );
#889=LINE ( 'NONE', #3543, #2783 ) ;
#896=DIRECTION ( 'NONE',  ( -0.000000000000000000, -0.000000000000000000, 1.000000000000000000 ) ) ;
#897=LINE ( 'NONE', #3421, #3661 ) ;
#924=VECTOR ( 'NONE', #6380, 1000.000000000000000 ) ;
#931=DIRECTION ( 'NONE',  ( 0.000000000000000000, 0.000000000000000000, 1.000000000000000000 ) ) ;
#932=ADVANCED_FACE ( 'NONE', ( #8459, #2497 ), #5699, .T. ) ;
#936=CARTESIAN_POINT ( 'NONE',  ( -5.000000000000000000, -5.000000000000000000, 42.00000000000000711 ) ) ;
#938=ORIENTED_EDGE ( 'NONE', *, *, #3732, .F. ) ;
#942=DIRECTION ( 'NONE',  ( 0.000000000000000000, 0.000000000000000000, -1.000000000000000000 ) ) ;
#943=( NAMED_UNIT ( * ) SI_UNIT ( $, .STERADIAN. ) SOLID_ANGLE_UNIT ( ) );
#944=ORIENTED_EDGE ( 'NONE', *, *, #7928, .F. ) ;
#975=PLANE ( 'NONE',  #4861 ) ;
#983=CARTESIAN_POINT ( 'NONE',  ( -10.00000000000000000, 1.224646799147353256E-15, 42.00000000000000711 ) ) ;
#1011=CARTESIAN_POINT ( 'NONE',  ( 0.000000000000000000, 0.000000000000000000, 42.00000000000000711 ) ) ;
#1018=DIRECTION ( 'NONE',  ( -0.000000000000000000, -0.000000000000000000, 1.000000000000000000 ) ) ;
#1030=CIRCLE ( 'NONE', #7985, 10.00000000000000000 ) ;
#1032=DIRECTION ( 'NONE',  ( -1.734723475976806848E-16, -1.000000000000000000, 0.000000000000000000 ) ) ;
#1038=AXIS2_PLACEMENT_3D ( 'NONE', #8058, #6557, #6521 ) ;
#1041=LINE ( 'NONE', #335, #4655 ) ;
#1053=PLANE ( 'NONE',  #7902 ) ;
#1063=ORIENTED_EDGE ( 'NONE', *, *, #1301, .F. ) ;
#1093=EDGE_CURVE ( 'NONE', #1691, #6087, #7352, .T. ) ;
#1103=CARTESIAN_POINT ( 'NONE',  ( 0.000000000000000000, 0.000000000000000000, 120.0000000000000142 ) ) ;
#1137=DIRECTION ( 'NONE',  ( 0.000000000000000000, -0.000000000000000000, 1.000000000000000000 ) ) ;
#1155=DIRECTION ( 'NONE',  ( -1.000000000000000000, 0.000000000000000000, 0.000000000000000000 ) ) ;
#1194=CARTESIAN_POINT ( 'NONE',  ( -5.000000000000001776, 5.000000000000001776, 148.0000000000000284 ) ) ;
#1201=VECTOR ( 'NONE', #7955, 1000.000000000000000 ) ;
#1205=CARTESIAN_POINT ( 'NONE',  ( 5.000000000000000000, 5.000000000000000000, 34.00000000000000711 ) ) ;
#1206=ORIENTED_EDGE ( 'NONE', *, *, #7099, .F. ) ;
#1217=ORIENTED_EDGE ( 'NONE', *, *, #8059, .F. ) ;
#1249=LINE ( 'NONE', #3908, #3655 ) ;
#1253=ORIENTED_EDGE ( 'NONE', *, *, #2700, .T. ) ;
#1297=ORIENTED_EDGE ( 'NONE', *, *, #3064, .T. ) ;
#1301=EDGE_CURVE ( 'NONE', #1635, #478, #7525, .T. ) ;
#1307=ORIENTED_EDGE ( 'NONE', *, *, #88, .F. ) ;
#1310=FACE_BOUND ( 'NONE', #5483, .T. ) ;
#1322=ORIENTED_EDGE ( 'NONE', *, *, #4702, .F. ) ;
#1323=AXIS2_PLACEMENT_3D ( 'NONE', #7092, #3181, #3705 ) ;
#1333=CARTESIAN_POINT ( 'NONE',  ( 0.000000000000000000, 0.000000000000000000, 62.00000000000001421 ) ) ;
#1348=EDGE_CURVE ( 'NONE', #4522, #2939, #1041, .T. ) ;
#1353=DIRECTION ( 'NONE',  ( 0.000000000000000000, 0.000000000000000000, 1.000000000000000000 ) ) ;
#1382=CIRCLE ( 'NONE', #687, 10.00000000000000000 ) ;
#1399=VERTEX_POINT ( 'NONE', #7708 ) ;
#1454=EDGE_CURVE ( 'NONE', #5984, #4522, #3386, .T. ) ;
#1464=DIRECTION ( 'NONE',  ( -0.000000000000000000, -0.000000000000000000, -1.000000000000000000 ) ) ;
#1503=FACE_OUTER_BOUND ( 'NONE', #8063, .T. ) ;
#1523=FILL_AREA_STYLE_COLOUR ( '', #6540 ) ;
#1524=DIRECTION ( 'NONE',  ( -1.734723475976806848E-16, -1.000000000000000000, 0.000000000000000000 ) ) ;
#1527=CARTESIAN_POINT ( 'NONE',  ( 0.000000000000000000, 0.000000000000000000, 42.00000000000000711 ) ) ;
#1541=CARTESIAN_POINT ( 'NONE',  ( -5.000000000000000000, -5.000000000000000000, 148.0000000000000284 ) ) ;
#1576=MECHANICAL_DESIGN_GEOMETRIC_PRESENTATION_REPRESENTATION('',(#7272),#887);
#1594=CARTESIAN_POINT ( 'NONE',  ( 0.000000000000000000, 0.000000000000000000, 62.00000000000001421 ) ) ;
#1598=DIRECTION ( 'NONE',  ( -1.000000000000000000, 0.000000000000000000, -0.000000000000000000 ) ) ;
#1615=ADVANCED_FACE ( 'NONE', ( #856 ), #5589, .F. ) ;
#1619=AXIS2_PLACEMENT_3D ( 'NONE', #1333, #4777, #8096 ) ;
#1635=VERTEX_POINT ( 'NONE', #4857 ) ;
#1636=EDGE_LOOP ( 'NONE', ( #1253, #4981 ) ) ;
#1672=CYLINDRICAL_SURFACE ( 'NONE', #4610, 20.00000000000000000 ) ;
#1679=ORIENTED_EDGE ( 'NONE', *, *, #6271, .F. ) ;
#1689=DIRECTION ( 'NONE',  ( -1.000000000000000000, 0.000000000000000000, 0.000000000000000000 ) ) ;
#1690=EDGE_LOOP ( 'NONE', ( #2075, #8055, #779, #8237 ) ) ;
#1691=VERTEX_POINT ( 'NONE', #7608 ) ;
#1692=LINE ( 'NONE', #5598, #7026 ) ;
#1703=ORIENTED_EDGE ( 'NONE', *, *, #6279, .T. ) ;
#1713=VECTOR ( 'NONE', #2844, 1000.000000000000000 ) ;
#1721=VECTOR ( 'NONE', #7839, 1000.000000000000000 ) ;
#1741=CARTESIAN_POINT ( 'NONE',  ( 5.000000000000000000, -5.000000000000000000, 34.00000000000000711 ) ) ;
#1757=AXIS2_PLACEMENT_3D ( 'NONE', #6982, #1032, #2515 ) ;
#1801=ORIENTED_EDGE ( 'NONE', *, *, #2256, .F. ) ;
#1809=ORIENTED_EDGE ( 'NONE', *, *, #8227, .T. ) ;
#1812=ADVANCED_FACE ( 'NONE', ( #6289 ), #7739, .F. ) ;
#1825=PRODUCT_DEFINITION ( 'UNKNOWN', '', #719, #6547 ) ;
#1828=VERTEX_POINT ( 'NONE', #7073 ) ;
#1836=MECHANICAL_DESIGN_GEOMETRIC_PRESENTATION_REPRESENTATION('',(#7674),#3914);
#1838=ORIENTED_EDGE ( 'NONE', *, *, #5815, .T. ) ;
#1868=CARTESIAN_POINT ( 'NONE',  ( -5.000000000000000000, -5.000000000000000000, 140.0000000000000000 ) ) ;
#1876=CIRCLE ( 'NONE', #608, 10.00000000000000000 ) ;
#1917=VERTEX_POINT ( 'NONE', #8513 ) ;
#1933=DIRECTION ( 'NONE',  ( -1.000000000000000000, 0.000000000000000000, -0.000000000000000000 ) ) ;
#1935=LINE ( 'NONE', #6496, #3584 ) ;
#2062=CARTESIAN_POINT ( 'NONE',  ( 5.000000000000000000, -5.000000000000000000, 148.0000000000000284 ) ) ;
#2067=CARTESIAN_POINT ( 'NONE',  ( -5.000000000000001776, 5.000000000000001776, 34.00000000000000711 ) ) ;
#2075=ORIENTED_EDGE ( 'NONE', *, *, #1348, .T. ) ;
#2081=DIRECTION ( 'NONE',  ( 1.000000000000000000, 0.000000000000000000, 0.000000000000000000 ) ) ;
#2104=DIRECTION ( 'NONE',  ( 0.000000000000000000, 0.000000000000000000, -1.000000000000000000 ) ) ;
#2114=VECTOR ( 'NONE', #6534, 1000.000000000000000 ) ;
#2117=VECTOR ( 'NONE', #5392, 1000.000000000000000 ) ;
#2141=ORIENTED_EDGE ( 'NONE', *, *, #6559, .F. ) ;
#2145=DIRECTION ( 'NONE',  ( -1.000000000000000000, 0.000000000000000000, 0.000000000000000000 ) ) ;
#2179=( LENGTH_UNIT ( ) NAMED_UNIT ( * ) SI_UNIT ( .MILLI., .METRE. ) );
#2197=DIRECTION ( 'NONE',  ( 1.000000000000000000, 0.000000000000000000, 0.000000000000000000 ) ) ;
#2225=ORIENTED_EDGE ( 'NONE', *, *, #3672, .F. ) ;
#2237=LINE ( 'NONE', #6361, #2813 ) ;
#2239=DIRECTION ( 'NONE',  ( -1.734723475976806848E-16, 1.000000000000000000, 0.000000000000000000 ) ) ;
#2256=EDGE_CURVE ( 'NONE', #5747, #5984, #1935, .T. ) ;
#2272=( NAMED_UNIT ( * ) PLANE_ANGLE_UNIT ( ) SI_UNIT ( $, .RADIAN. ) );
#2298=DIRECTION ( 'NONE',  ( -1.000000000000000000, 0.000000000000000000, 0.000000000000000000 ) ) ;
#2334=ADVANCED_FACE ( 'NONE', ( #7889, #8074 ), #6047, .T. ) ;
#2388=UNCERTAINTY_MEASURE_WITH_UNIT (LENGTH_MEASURE( 1.000000000000000082E-05 ), #2179, 'distance_accuracy_value', 'NONE');
#2398=DIRECTION ( 'NONE',  ( -1.000000000000000000, 0.000000000000000000, -0.000000000000000000 ) ) ;
#2497=FACE_OUTER_BOUND ( 'NONE', #1636, .T. ) ;
#2515=DIRECTION ( 'NONE',  ( 1.000000000000000000, -1.734723475976806848E-16, 0.000000000000000000 ) ) ;
#2544=VECTOR ( 'NONE', #7857, 1000.000000000000000 ) ;
#2566=VECTOR ( 'NONE', #3629, 1000.000000000000000 ) ;
#2568=ORIENTED_EDGE ( 'NONE', *, *, #4724, .T. ) ;
#2607=DIRECTION ( 'NONE',  ( -0.000000000000000000, -0.000000000000000000, 1.000000000000000000 ) ) ;
#2623=ORIENTED_EDGE ( 'NONE', *, *, #1454, .T. ) ;
#2646=ORIENTED_EDGE ( 'NONE', *, *, #7644, .F. ) ;
#2658=ADVANCED_FACE ( 'NONE', ( #8330 ), #1053, .F. ) ;
#2664=FACE_OUTER_BOUND ( 'NONE', #1690, .T. ) ;
#2678=CIRCLE ( 'NONE', #6695, 10.00000000000000000 ) ;
#2680=UNCERTAINTY_MEASURE_WITH_UNIT (LENGTH_MEASURE( 1.000000000000000082E-05 ), #7558, 'distance_accuracy_value', 'NONE');
#2683=AXIS2_PLACEMENT_3D ( 'NONE', #1527, #8114, #792 ) ;
#2687=ORIENTED_EDGE ( 'NONE', *, *, #2256, .T. ) ;
#2700=EDGE_CURVE ( 'NONE', #7614, #6221, #6646, .T. ) ;
#2726=DIRECTION ( 'NONE',  ( 1.000000000000000000, 0.000000000000000000, 0.000000000000000000 ) ) ;
#2748=DIRECTION ( 'NONE',  ( 1.000000000000000000, -1.734723475976806848E-16, 0.000000000000000000 ) ) ;
#2783=VECTOR ( 'NONE', #5536, 1000.000000000000000 ) ;
#2797=DIRECTION ( 'NONE',  ( 1.000000000000000000, 0.000000000000000000, 0.000000000000000000 ) ) ;
#2799=DIRECTION ( 'NONE',  ( 1.000000000000000000, 1.734723475976806848E-16, -0.000000000000000000 ) ) ;
#2800=LINE ( 'NONE', #5366, #5127 ) ;
#2813=VECTOR ( 'NONE', #931, 1000.000000000000000 ) ;
#2814=ORIENTED_EDGE ( 'NONE', *, *, #4099, .F. ) ;
#2844=DIRECTION ( 'NONE',  ( -1.000000000000000000, 0.000000000000000000, 0.000000000000000000 ) ) ;
#2904=ORIENTED_EDGE ( 'NONE', *, *, #6192, .T. ) ;
#2907=VECTOR ( 'NONE', #381, 1000.000000000000000 ) ;
#2929=CARTESIAN_POINT ( 'NONE',  ( -10.00000000000000000, 1.224646799147353256E-15, 62.00000000000001421 ) ) ;
#2934=ORIENTED_EDGE ( 'NONE', *, *, #7331, .F. ) ;
#2939=VERTEX_POINT ( 'NONE', #6118 ) ;
#2997=PLANE ( 'NONE',  #6856 ) ;
#3028=EDGE_LOOP ( 'NONE', ( #185, #4690, #2141, #1206 ) ) ;
#3064=EDGE_CURVE ( 'NONE', #6827, #5747, #3945, .T. ) ;
#3081=CARTESIAN_POINT ( 'NONE',  ( -5.000000000000000000, -5.000000000000000000, 140.0000000000000000 ) ) ;
#3082=LINE ( 'NONE', #1741, #5874 ) ;
#3117=DIRECTION ( 'NONE',  ( 0.000000000000000000, 0.000000000000000000, 1.000000000000000000 ) ) ;
#3122=ORIENTED_EDGE ( 'NONE', *, *, #5629, .F. ) ;
#3123=CARTESIAN_POINT ( 'NONE',  ( 0.000000000000000000, 0.000000000000000000, 0.000000000000000000 ) ) ;
#3163=EDGE_CURVE ( 'NONE', #6448, #5985, #2800, .T. ) ;
#3181=DIRECTION ( 'NONE',  ( 0.000000000000000000, 0.000000000000000000, -1.000000000000000000 ) ) ;
#3192=FACE_OUTER_BOUND ( 'NONE', #3907, .T. ) ;
#3224=EDGE_CURVE ( 'NONE', #6827, #4339, #3388, .T. ) ;
#3241=AXIS2_PLACEMENT_3D ( 'NONE', #7831, #6550, #685 ) ;
#3256=EDGE_LOOP ( 'NONE', ( #7714, #4397, #585, #7095 ) ) ;
#3262=VERTEX_POINT ( 'NONE', #49 ) ;
#3263=LINE ( 'NONE', #3964, #5457 ) ;
#3285=CARTESIAN_POINT ( 'NONE',  ( -20.00000000000000000, 2.449293598294706513E-15, 62.00000000000001421 ) ) ;
#3290=VERTEX_POINT ( 'NONE', #3285 ) ;
#3341=EDGE_LOOP ( 'NONE', ( #5683, #3122, #1063, #7198 ) ) ;
#3378=FACE_OUTER_BOUND ( 'NONE', #8575, .T. ) ;
#3382=EDGE_CURVE ( 'NONE', #3653, #4789, #8210, .T. ) ;
#3386=LINE ( 'NONE', #5333, #1201 ) ;
#3388=LINE ( 'NONE', #7428, #8250 ) ;
#3421=CARTESIAN_POINT ( 'NONE',  ( 5.000000000000000000, 5.000000000000000000, 34.00000000000000711 ) ) ;
#3451=CARTESIAN_POINT ( 'NONE',  ( 0.000000000000000000, 0.000000000000000000, -14.56854249492377207 ) ) ;
#3487=ORIENTED_EDGE ( 'NONE', *, *, #3672, .T. ) ;
#3506=LINE ( 'NONE', #97, #7277 ) ;
#3521=CIRCLE ( 'NONE', #3241, 10.00000000000000000 ) ;
#3529=VERTEX_POINT ( 'NONE', #4530 ) ;
#3543=CARTESIAN_POINT ( 'NONE',  ( -5.000000000000000000, -5.000000000000000000, 34.00000000000000711 ) ) ;
#3550=DIRECTION ( 'NONE',  ( 0.000000000000000000, -1.000000000000000000, 0.000000000000000000 ) ) ;
#3584=VECTOR ( 'NONE', #7439, 1000.000000000000000 ) ;
#3593=LINE ( 'NONE', #983, #2566 ) ;
#3629=DIRECTION ( 'NONE',  ( -0.000000000000000000, -0.000000000000000000, 1.000000000000000000 ) ) ;
#3653=VERTEX_POINT ( 'NONE', #755 ) ;
#3655=VECTOR ( 'NONE', #2607, 1000.000000000000000 ) ;
#3661=VECTOR ( 'NONE', #3550, 1000.000000000000000 ) ;
#3672=EDGE_CURVE ( 'NONE', #5766, #1691, #4575, .T. ) ;
#3705=DIRECTION ( 'NONE',  ( -1.000000000000000000, 0.000000000000000000, -0.000000000000000000 ) ) ;
#3731=DIRECTION ( 'NONE',  ( -0.000000000000000000, -0.000000000000000000, -1.000000000000000000 ) ) ;
#3732=EDGE_CURVE ( 'NONE', #6221, #7614, #1382, .T. ) ;
#3739=DIRECTION ( 'NONE',  ( 1.000000000000000000, 0.000000000000000000, 0.000000000000000000 ) ) ;
#3748=EDGE_CURVE ( 'NONE', #8592, #5790, #6965, .T. ) ;
#3767=ORIENTED_EDGE ( 'NONE', *, *, #7899, .F. ) ;
#3809=VECTOR ( 'NONE', #1155, 1000.000000000000000 ) ;
#3813=CARTESIAN_POINT ( 'NONE',  ( 0.000000000000000000, 0.000000000000000000, 120.0000000000000142 ) ) ;
#3824=DIRECTION ( 'NONE',  ( -0.000000000000000000, -0.000000000000000000, 1.000000000000000000 ) ) ;
#3853=LINE ( 'NONE', #1194, #2114 ) ;
#3880=AXIS2_PLACEMENT_3D ( 'NONE', #4403, #7053, #6446 ) ;
#3895=AXIS2_PLACEMENT_3D ( 'NONE', #7501, #1018, #2197 ) ;
#3907=EDGE_LOOP ( 'NONE', ( #4374, #2568 ) ) ;
#3908=CARTESIAN_POINT ( 'NONE',  ( -10.00000000000000000, 1.224646799147353256E-15, 42.00000000000000711 ) ) ;
#3914=( GEOMETRIC_REPRESENTATION_CONTEXT ( 3 ) GLOBAL_UNCERTAINTY_ASSIGNED_CONTEXT ( ( #4377 ) ) GLOBAL_UNIT_ASSIGNED_CONTEXT ( ( #115, #8191, #6872 ) ) REPRESENTATION_CONTEXT ( 'NONE', 'WORKASPACE' ) );
#3916=PLANE ( 'NONE',  #1038 ) ;
#3945=LINE ( 'NONE', #7196, #2907 ) ;
#3964=CARTESIAN_POINT ( 'NONE',  ( 5.000000000000000000, 5.000000000000000000, 34.00000000000000711 ) ) ;
#4013=CARTESIAN_POINT ( 'NONE',  ( -20.00000000000000000, 2.449293598294706513E-15, 120.0000000000000142 ) ) ;
#4014=ADVANCED_FACE ( 'NONE', ( #129 ), #5623, .T. ) ;
#4066=ADVANCED_FACE ( 'NONE', ( #4801 ), #975, .F. ) ;
#4072=ORIENTED_EDGE ( 'NONE', *, *, #5998, .F. ) ;
#4099=EDGE_CURVE ( 'NONE', #5237, #3653, #889, .T. ) ;
#4105=CARTESIAN_POINT ( 'NONE',  ( 0.000000000000000000, 0.000000000000000000, 120.0000000000000142 ) ) ;
#4118=DIRECTION ( 'NONE',  ( -0.000000000000000000, 0.000000000000000000, 1.000000000000000000 ) ) ;
#4125=ORIENTED_EDGE ( 'NONE', *, *, #5998, .T. ) ;
#4130=DIRECTION ( 'NONE',  ( 0.000000000000000000, 0.000000000000000000, 1.000000000000000000 ) ) ;
#4143=CARTESIAN_POINT ( 'NONE',  ( 5.000000000000000000, 5.000000000000000000, 42.00000000000000711 ) ) ;
#4153=DIRECTION ( 'NONE',  ( -0.000000000000000000, -0.000000000000000000, 1.000000000000000000 ) ) ;
#4161=VECTOR ( 'NONE', #2239, 1000.000000000000000 ) ;
#4174=SURFACE_STYLE_FILL_AREA ( #6739 ) ;
#4185=CARTESIAN_POINT ( 'NONE',  ( 0.000000000000000000, 0.000000000000000000, 62.00000000000001421 ) ) ;
#4196=DIRECTION ( 'NONE',  ( 1.000000000000000000, 1.734723475976806848E-16, 0.000000000000000000 ) ) ;
#4221=( NAMED_UNIT ( * ) SI_UNIT ( $, .STERADIAN. ) SOLID_ANGLE_UNIT ( ) );
#4270=VECTOR ( 'NONE', #6735, 1000.000000000000000 ) ;
#4285=ORIENTED_EDGE ( 'NONE', *, *, #1348, .F. ) ;
#4315=CARTESIAN_POINT ( 'NONE',  ( 5.000000000000000000, -5.000000000000000000, 34.00000000000000711 ) ) ;
#4332=ADVANCED_FACE ( 'NONE', ( #444 ), #5014, .T. ) ;
#4339=VERTEX_POINT ( 'NONE', #6956 ) ;
#4374=ORIENTED_EDGE ( 'NONE', *, *, #6559, .T. ) ;
#4377=UNCERTAINTY_MEASURE_WITH_UNIT (LENGTH_MEASURE( 1.000000000000000082E-05 ), #115, 'distance_accuracy_value', 'NONE');
#4397=ORIENTED_EDGE ( 'NONE', *, *, #6376, .T. ) ;
#4403=CARTESIAN_POINT ( 'NONE',  ( 0.000000000000000000, 0.000000000000000000, 42.00000000000000711 ) ) ;
#4414=EDGE_LOOP ( 'NONE', ( #7777, #7162 ) ) ;
#4522=VERTEX_POINT ( 'NONE', #7252 ) ;
#4527=AXIS2_PLACEMENT_3D ( 'NONE', #7610, #240, #1689 ) ;
#4530=CARTESIAN_POINT ( 'NONE',  ( 5.000000000000000000, -5.000000000000000000, 34.00000000000000711 ) ) ;
#4535=DIRECTION ( 'NONE',  ( 0.000000000000000000, 0.000000000000000000, 1.000000000000000000 ) ) ;
#4556=EDGE_LOOP ( 'NONE', ( #6226, #5462, #8420, #3767 ) ) ;
#4575=CIRCLE ( 'NONE', #4714, 10.00000000000000000 ) ;
#4610=AXIS2_PLACEMENT_3D ( 'NONE', #3451, #127, #2797 ) ;
#4623=CARTESIAN_POINT ( 'NONE',  ( -5.000000000000001776, 5.000000000000001776, 42.00000000000000711 ) ) ;
#4627=DIRECTION ( 'NONE',  ( 0.000000000000000000, 1.000000000000000000, 0.000000000000000000 ) ) ;
#4655=VECTOR ( 'NONE', #5162, 1000.000000000000000 ) ;
#4690=ORIENTED_EDGE ( 'NONE', *, *, #8088, .T. ) ;
#4693=FACE_OUTER_BOUND ( 'NONE', #6437, .T. ) ;
#4700=ORIENTED_EDGE ( 'NONE', *, *, #1301, .T. ) ;
#4702=EDGE_CURVE ( 'NONE', #5985, #6827, #3853, .T. ) ;
#4706=SHAPE_REPRESENTATION ( 'roller axis assy_r6', ( #594 ), #8234 ) ;
#4714=AXIS2_PLACEMENT_3D ( 'NONE', #4105, #7936, #6575 ) ;
#4724=EDGE_CURVE ( 'NONE', #628, #3262, #8511, .T. ) ;
#4755=LINE ( 'NONE', #2067, #6558 ) ;
#4762=ORIENTED_EDGE ( 'NONE', *, *, #3224, .T. ) ;
#4776=DIRECTION ( 'NONE',  ( -0.000000000000000000, -0.000000000000000000, 1.000000000000000000 ) ) ;
#4777=DIRECTION ( 'NONE',  ( -0.000000000000000000, -0.000000000000000000, 1.000000000000000000 ) ) ;
#4788=PLANE ( 'NONE',  #5727 ) ;
#4789=VERTEX_POINT ( 'NONE', #5269 ) ;
#4801=FACE_OUTER_BOUND ( 'NONE', #6258, .T. ) ;
#4857=CARTESIAN_POINT ( 'NONE',  ( -5.000000000000001776, 5.000000000000001776, 34.00000000000000711 ) ) ;
#4861=AXIS2_PLACEMENT_3D ( 'NONE', #1541, #2799, #6846 ) ;
#4876=ORIENTED_EDGE ( 'NONE', *, *, #3382, .T. ) ;
#4883=DIRECTION ( 'NONE',  ( -1.000000000000000000, 0.000000000000000000, 0.000000000000000000 ) ) ;
#4911=AXIS2_PLACEMENT_3D ( 'NONE', #8222, #4776, #2081 ) ;
#4915=CIRCLE ( 'NONE', #37, 10.00000000000000000 ) ;
#4918=ORIENTED_EDGE ( 'NONE', *, *, #7331, .T. ) ;
#4940=ADVANCED_FACE ( 'NONE', ( #6184 ), #1672, .T. ) ;
#4942=LINE ( 'NONE', #366, #3809 ) ;
#4960=AXIS2_PLACEMENT_3D ( 'NONE', #1103, #5225, #5058 ) ;
#4977=AXIS2_PLACEMENT_3D ( 'NONE', #7224, #7320, #1933 ) ;
#4981=ORIENTED_EDGE ( 'NONE', *, *, #3732, .T. ) ;
#5014=CYLINDRICAL_SURFACE ( 'NONE', #7091, 20.00000000000000000 ) ;
#5025=ORIENTED_EDGE ( 'NONE', *, *, #8072, .T. ) ;
#5058=DIRECTION ( 'NONE',  ( 1.000000000000000000, 0.000000000000000000, -0.000000000000000000 ) ) ;
#5089=CARTESIAN_POINT ( 'NONE',  ( -5.000000000000001776, 5.000000000000001776, 148.0000000000000284 ) ) ;
#5124=CARTESIAN_POINT ( 'NONE',  ( -5.000000000000001776, 5.000000000000001776, 34.00000000000000711 ) ) ;
#5127=VECTOR ( 'NONE', #4627, 1000.000000000000000 ) ;
#5152=LINE ( 'NONE', #4623, #2544 ) ;
#5162=DIRECTION ( 'NONE',  ( 0.000000000000000000, 1.000000000000000000, 0.000000000000000000 ) ) ;
#5171=CARTESIAN_POINT ( 'NONE',  ( -5.000000000000000000, -5.000000000000000000, 34.00000000000000711 ) ) ;
#5186=PLANE ( 'NONE',  #4960 ) ;
#5202=CARTESIAN_POINT ( 'NONE',  ( 10.00000000000000000, 0.000000000000000000, 140.0000000000000000 ) ) ;
#5206=EDGE_LOOP ( 'NONE', ( #8184, #5627, #1297, #1838 ) ) ;
#5225=DIRECTION ( 'NONE',  ( 0.000000000000000000, 0.000000000000000000, 1.000000000000000000 ) ) ;
#5237=VERTEX_POINT ( 'NONE', #6042 ) ;
#5255=CARTESIAN_POINT ( 'NONE',  ( 10.00000000000000000, 0.000000000000000000, 42.00000000000000711 ) ) ;
#5269=CARTESIAN_POINT ( 'NONE',  ( -5.000000000000001776, 5.000000000000001776, 42.00000000000000711 ) ) ;
#5281=CARTESIAN_POINT ( 'NONE',  ( 5.000000000000000000, 5.000000000000000000, 148.0000000000000284 ) ) ;
#5333=CARTESIAN_POINT ( 'NONE',  ( -5.000000000000000000, -5.000000000000000000, 140.0000000000000000 ) ) ;
#5334=ADVANCED_FACE ( 'NONE', ( #833 ), #6263, .T. ) ;
#5341=VECTOR ( 'NONE', #507, 1000.000000000000000 ) ;
#5353=PLANE ( 'NONE',  #227 ) ;
#5360=CIRCLE ( 'NONE', #1619, 20.00000000000000000 ) ;
#5366=CARTESIAN_POINT ( 'NONE',  ( 5.000000000000000000, -5.000000000000000000, 148.0000000000000284 ) ) ;
#5386=CARTESIAN_POINT ( 'NONE',  ( -5.000000000000000000, -5.000000000000000000, 148.0000000000000284 ) ) ;
#5392=DIRECTION ( 'NONE',  ( -0.000000000000000000, -0.000000000000000000, -1.000000000000000000 ) ) ;
#5400=ORIENTED_EDGE ( 'NONE', *, *, #1093, .T. ) ;
#5415=ADVANCED_BREP_SHAPE_REPRESENTATION ( '', ( #7589, #594 ), #8234 ) ;
#5457=VECTOR ( 'NONE', #7919, 1000.000000000000000 ) ;
#5462=ORIENTED_EDGE ( 'NONE', *, *, #7639, .F. ) ;
#5483=EDGE_LOOP ( 'NONE', ( #4285, #8279, #4072, #690 ) ) ;
#5499=AXIS2_PLACEMENT_3D ( 'NONE', #6158, #1598, #4118 ) ;
#5514=DIRECTION ( 'NONE',  ( 1.000000000000000000, 0.000000000000000000, 0.000000000000000000 ) ) ;
#5530=ORIENTED_EDGE ( 'NONE', *, *, #5641, .T. ) ;
#5536=DIRECTION ( 'NONE',  ( -0.000000000000000000, -0.000000000000000000, 1.000000000000000000 ) ) ;
#5555=CARTESIAN_POINT ( 'NONE',  ( -5.000000000000000000, -5.000000000000000000, 148.0000000000000284 ) ) ;
#5589=PLANE ( 'NONE',  #5499 ) ;
#5598=CARTESIAN_POINT ( 'NONE',  ( 5.000000000000000000, -5.000000000000000000, 148.0000000000000284 ) ) ;
#5618=DIRECTION ( 'NONE',  ( 0.000000000000000000, 0.000000000000000000, -1.000000000000000000 ) ) ;
#5623=CYLINDRICAL_SURFACE ( 'NONE', #3895, 10.00000000000000000 ) ;
#5627=ORIENTED_EDGE ( 'NONE', *, *, #4702, .T. ) ;
#5629=EDGE_CURVE ( 'NONE', #478, #8592, #3263, .T. ) ;
#5641=EDGE_CURVE ( 'NONE', #5237, #1635, #7175, .T. ) ;
#5683=ORIENTED_EDGE ( 'NONE', *, *, #7899, .T. ) ;
#5699=PLANE ( 'NONE',  #1323 ) ;
#5727=AXIS2_PLACEMENT_3D ( 'NONE', #158, #1524, #2748 ) ;
#5744=DIRECTION ( 'NONE',  ( 0.000000000000000000, 1.000000000000000000, 0.000000000000000000 ) ) ;
#5747=VERTEX_POINT ( 'NONE', #5555 ) ;
#5754=VECTOR ( 'NONE', #4130, 1000.000000000000000 ) ;
#5756=DIRECTION ( 'NONE',  ( 0.000000000000000000, 0.000000000000000000, 1.000000000000000000 ) ) ;
#5763=EDGE_LOOP ( 'NONE', ( #938, #155, #1703, #6048 ) ) ;
#5764=DIRECTION ( 'NONE',  ( 1.000000000000000000, 0.000000000000000000, 0.000000000000000000 ) ) ;
#5766=VERTEX_POINT ( 'NONE', #198 ) ;
#5790=VERTEX_POINT ( 'NONE', #7434 ) ;
#5815=EDGE_CURVE ( 'NONE', #5747, #6448, #6777, .T. ) ;
#5874=VECTOR ( 'NONE', #3824, 1000.000000000000000 ) ;
#5913=EDGE_CURVE ( 'NONE', #6448, #4522, #1692, .T. ) ;
#5941=EDGE_LOOP ( 'NONE', ( #2646, #2225 ) ) ;
#5954=VECTOR ( 'NONE', #8291, 1000.000000000000000 ) ;
#5974=EDGE_LOOP ( 'NONE', ( #7805, #1307 ) ) ;
#5984=VERTEX_POINT ( 'NONE', #3081 ) ;
#5985=VERTEX_POINT ( 'NONE', #5281 ) ;
#5998=EDGE_CURVE ( 'NONE', #4339, #5984, #10, .T. ) ;
#6042=CARTESIAN_POINT ( 'NONE',  ( -5.000000000000000000, -5.000000000000000000, 34.00000000000000711 ) ) ;
#6047=PLANE ( 'NONE',  #4977 ) ;
#6048=ORIENTED_EDGE ( 'NONE', *, *, #6192, .F. ) ;
#6058=AXIS2_PLACEMENT_3D ( 'NONE', #6656, #8073, #7981 ) ;
#6063=CYLINDRICAL_SURFACE ( 'NONE', #756, 10.00000000000000000 ) ;
#6081=CARTESIAN_POINT ( 'NONE',  ( 5.000000000000000000, 5.000000000000000000, 148.0000000000000284 ) ) ;
#6087=VERTEX_POINT ( 'NONE', #5202 ) ;
#6092=LINE ( 'NONE', #128, #1713 ) ;
#6118=CARTESIAN_POINT ( 'NONE',  ( 5.000000000000000000, 5.000000000000000000, 140.0000000000000000 ) ) ;
#6126=ADVANCED_FACE ( 'NONE', ( #1503 ), #6063, .T. ) ;
#6139=CARTESIAN_POINT ( 'NONE',  ( 0.000000000000000000, 0.000000000000000000, 34.00000000000000711 ) ) ;
#6158=CARTESIAN_POINT ( 'NONE',  ( 5.000000000000000000, 5.000000000000000000, 34.00000000000000711 ) ) ;
#6171=ADVANCED_FACE ( 'NONE', ( #3378 ), #852, .F. ) ;
#6184=FACE_OUTER_BOUND ( 'NONE', #3028, .T. ) ;
#6192=EDGE_CURVE ( 'NONE', #7614, #1399, #3506, .T. ) ;
#6209=ORIENTED_EDGE ( 'NONE', *, *, #7639, .T. ) ;
#6218=SHAPE_REPRESENTATION_RELATIONSHIP ( 'NONE' , 'NONE' ,  #4706, #5415 ) ;
#6221=VERTEX_POINT ( 'NONE', #187 ) ;
#6226=ORIENTED_EDGE ( 'NONE', *, *, #3382, .F. ) ;
#6240=ORIENTED_EDGE ( 'NONE', *, *, #88, .T. ) ;
#6258=EDGE_LOOP ( 'NONE', ( #4125, #1801, #7860, #4762 ) ) ;
#6263=CYLINDRICAL_SURFACE ( 'NONE', #2683, 10.00000000000000000 ) ;
#6271=EDGE_CURVE ( 'NONE', #1828, #6087, #1876, .T. ) ;
#6279=EDGE_CURVE ( 'NONE', #8107, #1399, #1030, .T. ) ;
#6285=DIRECTION ( 'NONE',  ( 0.000000000000000000, 0.000000000000000000, -1.000000000000000000 ) ) ;
#6289=FACE_OUTER_BOUND ( 'NONE', #689, .T. ) ;
#6306=ORIENTED_EDGE ( 'NONE', *, *, #6376, .F. ) ;
#6361=CARTESIAN_POINT ( 'NONE',  ( -20.00000000000000000, 2.449293598294706513E-15, -14.56854249492377207 ) ) ;
#6376=EDGE_CURVE ( 'NONE', #5766, #1828, #3593, .T. ) ;
#6380=DIRECTION ( 'NONE',  ( -1.000000000000000000, 1.734723475976806848E-16, -0.000000000000000000 ) ) ;
#6437=EDGE_LOOP ( 'NONE', ( #2623, #139, #544, #2687 ) ) ;
#6446=DIRECTION ( 'NONE',  ( -1.000000000000000000, 0.000000000000000000, 0.000000000000000000 ) ) ;
#6448=VERTEX_POINT ( 'NONE', #7774 ) ;
#6489=ORIENTED_EDGE ( 'NONE', *, *, #5641, .F. ) ;
#6496=CARTESIAN_POINT ( 'NONE',  ( -5.000000000000000000, -5.000000000000000000, 148.0000000000000284 ) ) ;
#6521=DIRECTION ( 'NONE',  ( 0.000000000000000000, -0.000000000000000000, 1.000000000000000000 ) ) ;
#6534=DIRECTION ( 'NONE',  ( -1.000000000000000000, 1.734723475976806848E-16, -0.000000000000000000 ) ) ;
#6540=COLOUR_RGB ( '',0.8941176470588234615, 0.8941176470588234615, 0.8941176470588234615 ) ;
#6543=ORIENTED_EDGE ( 'NONE', *, *, #3748, .T. ) ;
#6547=PRODUCT_DEFINITION_CONTEXT ( 'detailed design', #7470, 'design' ) ;
#6550=DIRECTION ( 'NONE',  ( 0.000000000000000000, 0.000000000000000000, -1.000000000000000000 ) ) ;
#6557=DIRECTION ( 'NONE',  ( 0.000000000000000000, 1.000000000000000000, 0.000000000000000000 ) ) ;
#6558=VECTOR ( 'NONE', #178, 1000.000000000000000 ) ;
#6559=EDGE_CURVE ( 'NONE', #3262, #628, #7417, .T. ) ;
#6575=DIRECTION ( 'NONE',  ( 1.000000000000000000, 0.000000000000000000, 0.000000000000000000 ) ) ;
#6646=CIRCLE ( 'NONE', #3880, 10.00000000000000000 ) ;
#6656=CARTESIAN_POINT ( 'NONE',  ( 0.000000000000000000, 0.000000000000000000, 140.0000000000000000 ) ) ;
#6662=DIRECTION ( 'NONE',  ( 0.000000000000000000, 0.000000000000000000, -1.000000000000000000 ) ) ;
#6695=AXIS2_PLACEMENT_3D ( 'NONE', #4185, #6662, #6844 ) ;
#6707=PLANE ( 'NONE',  #724 ) ;
#6735=DIRECTION ( 'NONE',  ( -0.000000000000000000, -0.000000000000000000, 1.000000000000000000 ) ) ;
#6738=ORIENTED_EDGE ( 'NONE', *, *, #7099, .T. ) ;
#6739=FILL_AREA_STYLE ('',( #1523 ) ) ;
#6744=APPLICATION_CONTEXT ( 'automotive_design' ) ;
#6763=DIRECTION ( 'NONE',  ( -1.734723475976806848E-16, 1.000000000000000000, 0.000000000000000000 ) ) ;
#6777=LINE ( 'NONE', #5386, #7544 ) ;
#6778=LINE ( 'NONE', #7572, #5754 ) ;
#6827=VERTEX_POINT ( 'NONE', #5089 ) ;
#6844=DIRECTION ( 'NONE',  ( -1.000000000000000000, 0.000000000000000000, 0.000000000000000000 ) ) ;
#6846=DIRECTION ( 'NONE',  ( -1.734723475976806848E-16, 1.000000000000000000, 0.000000000000000000 ) ) ;
#6856=AXIS2_PLACEMENT_3D ( 'NONE', #509, #7660, #2398 ) ;
#6865=AXIS2_PLACEMENT_3D ( 'NONE', #7421, #4196, #6763 ) ;
#6872=( NAMED_UNIT ( * ) SI_UNIT ( $, .STERADIAN. ) SOLID_ANGLE_UNIT ( ) );
#6956=CARTESIAN_POINT ( 'NONE',  ( -5.000000000000001776, 5.000000000000001776, 140.0000000000000000 ) ) ;
#6965=LINE ( 'NONE', #4143, #5954 ) ;
#6982=CARTESIAN_POINT ( 'NONE',  ( -5.000000000000001776, 5.000000000000001776, 148.0000000000000284 ) ) ;
#7018=ADVANCED_FACE ( 'NONE', ( #4693 ), #3916, .F. ) ;
#7026=VECTOR ( 'NONE', #3731, 1000.000000000000000 ) ;
#7033=LINE ( 'NONE', #8181, #924 ) ;
#7040=CIRCLE ( 'NONE', #4527, 20.00000000000000000 ) ;
#7053=DIRECTION ( 'NONE',  ( 0.000000000000000000, 0.000000000000000000, -1.000000000000000000 ) ) ;
#7073=CARTESIAN_POINT ( 'NONE',  ( -10.00000000000000000, 1.224646799147353256E-15, 140.0000000000000000 ) ) ;
#7091=AXIS2_PLACEMENT_3D ( 'NONE', #8338, #7683, #3739 ) ;
#7092=CARTESIAN_POINT ( 'NONE',  ( 0.000000000000000000, 0.000000000000000000, 42.00000000000000711 ) ) ;
#7095=ORIENTED_EDGE ( 'NONE', *, *, #1093, .F. ) ;
#7099=EDGE_CURVE ( 'NONE', #1917, #3262, #6778, .T. ) ;
#7147=AXIS2_PLACEMENT_3D ( 'NONE', #8508, #4535, #7194 ) ;
#7156=DIRECTION ( 'NONE',  ( 1.000000000000000000, 0.000000000000000000, 0.000000000000000000 ) ) ;
#7162=ORIENTED_EDGE ( 'NONE', *, *, #6279, .F. ) ;
#7175=LINE ( 'NONE', #5171, #1721 ) ;
#7194=DIRECTION ( 'NONE',  ( 1.000000000000000000, 0.000000000000000000, 0.000000000000000000 ) ) ;
#7196=CARTESIAN_POINT ( 'NONE',  ( -5.000000000000000000, -5.000000000000000000, 148.0000000000000284 ) ) ;
#7198=ORIENTED_EDGE ( 'NONE', *, *, #8059, .T. ) ;
#7224=CARTESIAN_POINT ( 'NONE',  ( 0.000000000000000000, 0.000000000000000000, 62.00000000000001421 ) ) ;
#7252=CARTESIAN_POINT ( 'NONE',  ( 5.000000000000000000, -5.000000000000000000, 140.0000000000000000 ) ) ;
#7272=STYLED_ITEM('',(#8657),#7589);
#7277=VECTOR ( 'NONE', #896, 1000.000000000000000 ) ;
#7301=ORIENTED_EDGE ( 'NONE', *, *, #4099, .T. ) ;
#7305=VECTOR ( 'NONE', #7828, 1000.000000000000000 ) ;
#7306=CLOSED_SHELL ( 'NONE', ( #8542, #4940, #5334, #4014, #932, #6171, #8283, #1615, #2658, #8032, #2334, #567, #4332, #7365, #1812, #4066, #7018, #643, #710, #6126 ) ) ;
#7320=DIRECTION ( 'NONE',  ( 0.000000000000000000, 0.000000000000000000, -1.000000000000000000 ) ) ;
#7331=EDGE_CURVE ( 'NONE', #3529, #5790, #3082, .T. ) ;
#7352=LINE ( 'NONE', #5255, #4270 ) ;
#7365=ADVANCED_FACE ( 'NONE', ( #7786 ), #2997, .F. ) ;
#7383=FACE_OUTER_BOUND ( 'NONE', #3256, .T. ) ;
#7417=CIRCLE ( 'NONE', #7147, 20.00000000000000000 ) ;
#7421=CARTESIAN_POINT ( 'NONE',  ( -5.000000000000000000, -5.000000000000000000, 34.00000000000000711 ) ) ;
#7428=CARTESIAN_POINT ( 'NONE',  ( -5.000000000000001776, 5.000000000000001776, 148.0000000000000284 ) ) ;
#7432=ORIENTED_EDGE ( 'NONE', *, *, #8469, .F. ) ;
#7434=CARTESIAN_POINT ( 'NONE',  ( 5.000000000000000000, -5.000000000000000000, 42.00000000000000711 ) ) ;
#7439=DIRECTION ( 'NONE',  ( -0.000000000000000000, -0.000000000000000000, -1.000000000000000000 ) ) ;
#7441=PRESENTATION_STYLE_ASSIGNMENT (( #788 ) ) ;
#7464=PRODUCT ( 'roller axis assy_r6', 'roller axis assy_r6', '', ( #7631 ) ) ;
#7470=APPLICATION_CONTEXT ( 'automotive_design' ) ;
#7486=FACE_OUTER_BOUND ( 'NONE', #3341, .T. ) ;
#7501=CARTESIAN_POINT ( 'NONE',  ( 0.000000000000000000, 0.000000000000000000, 42.00000000000000711 ) ) ;
#7525=LINE ( 'NONE', #5124, #7305 ) ;
#7544=VECTOR ( 'NONE', #5514, 1000.000000000000000 ) ;
#7553=EDGE_CURVE ( 'NONE', #478, #3529, #897, .T. ) ;
#7558=( LENGTH_UNIT ( ) NAMED_UNIT ( * ) SI_UNIT ( .MILLI., .METRE. ) );
#7572=CARTESIAN_POINT ( 'NONE',  ( 20.00000000000000000, 0.000000000000000000, -14.56854249492377207 ) ) ;
#7589=MANIFOLD_SOLID_BREP ( 'Boss-Extrude4', #7306 ) ;
#7608=CARTESIAN_POINT ( 'NONE',  ( 10.00000000000000000, 0.000000000000000000, 120.0000000000000142 ) ) ;
#7610=CARTESIAN_POINT ( 'NONE',  ( 0.000000000000000000, 0.000000000000000000, 62.00000000000001421 ) ) ;
#7614=VERTEX_POINT ( 'NONE', #410 ) ;
#7631=PRODUCT_CONTEXT ( 'NONE', #6744, 'mechanical' ) ;
#7639=EDGE_CURVE ( 'NONE', #5790, #3653, #4942, .T. ) ;
#7644=EDGE_CURVE ( 'NONE', #1691, #5766, #4915, .T. ) ;
#7647=CARTESIAN_POINT ( 'NONE',  ( 0.000000000000000000, 0.000000000000000000, 140.0000000000000000 ) ) ;
#7657=ORIENTED_EDGE ( 'NONE', *, *, #2700, .F. ) ;
#7660=DIRECTION ( 'NONE',  ( 0.000000000000000000, 0.000000000000000000, -1.000000000000000000 ) ) ;
#7674=STYLED_ITEM ( 'NONE', ( #7441 ), #5415 ) ;
#7678=SHAPE_DEFINITION_REPRESENTATION ( #153, #4706 ) ;
#7683=DIRECTION ( 'NONE',  ( 0.000000000000000000, 0.000000000000000000, 1.000000000000000000 ) ) ;
#7708=CARTESIAN_POINT ( 'NONE',  ( 10.00000000000000000, 0.000000000000000000, 62.00000000000001421 ) ) ;
#7714=ORIENTED_EDGE ( 'NONE', *, *, #7644, .T. ) ;
#7739=PLANE ( 'NONE',  #1757 ) ;
#7774=CARTESIAN_POINT ( 'NONE',  ( 5.000000000000000000, -5.000000000000000000, 148.0000000000000284 ) ) ;
#7777=ORIENTED_EDGE ( 'NONE', *, *, #8072, .F. ) ;
#7786=FACE_OUTER_BOUND ( 'NONE', #5206, .T. ) ;
#7794=EDGE_LOOP ( 'NONE', ( #6209, #2814, #944, #4918 ) ) ;
#7805=ORIENTED_EDGE ( 'NONE', *, *, #253, .F. ) ;
#7828=DIRECTION ( 'NONE',  ( 1.000000000000000000, -1.734723475976806848E-16, 0.000000000000000000 ) ) ;
#7831=CARTESIAN_POINT ( 'NONE',  ( 0.000000000000000000, 0.000000000000000000, 140.0000000000000000 ) ) ;
#7835=ORIENTED_EDGE ( 'NONE', *, *, #4724, .F. ) ;
#7837=EDGE_LOOP ( 'NONE', ( #7432, #1679 ) ) ;
#7839=DIRECTION ( 'NONE',  ( -1.734723475976806848E-16, 1.000000000000000000, 0.000000000000000000 ) ) ;
#7857=DIRECTION ( 'NONE',  ( 1.000000000000000000, -1.734723475976806848E-16, 0.000000000000000000 ) ) ;
#7860=ORIENTED_EDGE ( 'NONE', *, *, #3064, .F. ) ;
#7874=EDGE_LOOP ( 'NONE', ( #6543, #2934, #8442, #8343 ) ) ;
#7889=FACE_BOUND ( 'NONE', #4414, .T. ) ;
#7899=EDGE_CURVE ( 'NONE', #4789, #8592, #5152, .T. ) ;
#7902=AXIS2_PLACEMENT_3D ( 'NONE', #4315, #5744, #1137 ) ;
#7919=DIRECTION ( 'NONE',  ( -0.000000000000000000, -0.000000000000000000, 1.000000000000000000 ) ) ;
#7928=EDGE_CURVE ( 'NONE', #3529, #5237, #6092, .T. ) ;
#7936=DIRECTION ( 'NONE',  ( 0.000000000000000000, 0.000000000000000000, 1.000000000000000000 ) ) ;
#7955=DIRECTION ( 'NONE',  ( 1.000000000000000000, 0.000000000000000000, 0.000000000000000000 ) ) ;
#7981=DIRECTION ( 'NONE',  ( -1.000000000000000000, 0.000000000000000000, -0.000000000000000000 ) ) ;
#7985=AXIS2_PLACEMENT_3D ( 'NONE', #1594, #942, #2298 ) ;
#7996=ORIENTED_EDGE ( 'NONE', *, *, #8088, .F. ) ;
#8029=ORIENTED_EDGE ( 'NONE', *, *, #8469, .T. ) ;
#8032=ADVANCED_FACE ( 'NONE', ( #8162 ), #6707, .T. ) ;
#8050=CARTESIAN_POINT ( 'NONE',  ( 5.000000000000000000, 5.000000000000000000, 42.00000000000000711 ) ) ;
#8055=ORIENTED_EDGE ( 'NONE', *, *, #8227, .F. ) ;
#8058=CARTESIAN_POINT ( 'NONE',  ( -5.000000000000000000, -5.000000000000000000, 148.0000000000000284 ) ) ;
#8059=EDGE_CURVE ( 'NONE', #1635, #4789, #4755, .T. ) ;
#8063=EDGE_LOOP ( 'NONE', ( #6306, #3487, #5400, #8029 ) ) ;
#8066=LINE ( 'NONE', #6081, #2117 ) ;
#8072=EDGE_CURVE ( 'NONE', #1399, #8107, #2678, .T. ) ;
#8073=DIRECTION ( 'NONE',  ( 0.000000000000000000, 0.000000000000000000, -1.000000000000000000 ) ) ;
#8074=FACE_OUTER_BOUND ( 'NONE', #5974, .T. ) ;
#8088=EDGE_CURVE ( 'NONE', #3290, #628, #2237, .T. ) ;
#8096=DIRECTION ( 'NONE',  ( -1.000000000000000000, 0.000000000000000000, 0.000000000000000000 ) ) ;
#8107=VERTEX_POINT ( 'NONE', #2929 ) ;
#8114=DIRECTION ( 'NONE',  ( -0.000000000000000000, -0.000000000000000000, 1.000000000000000000 ) ) ;
#8116=FACE_OUTER_BOUND ( 'NONE', #7837, .T. ) ;
#8138=CYLINDRICAL_SURFACE ( 'NONE', #4911, 10.00000000000000000 ) ;
#8162=FACE_OUTER_BOUND ( 'NONE', #325, .T. ) ;
#8174=( NAMED_UNIT ( * ) PLANE_ANGLE_UNIT ( ) SI_UNIT ( $, .RADIAN. ) );
#8179=ORIENTED_EDGE ( 'NONE', *, *, #8498, .F. ) ;
#8181=CARTESIAN_POINT ( 'NONE',  ( -5.000000000000001776, 5.000000000000001776, 140.0000000000000000 ) ) ;
#8184=ORIENTED_EDGE ( 'NONE', *, *, #3163, .T. ) ;
#8189=ORIENTED_EDGE ( 'NONE', *, *, #3224, .F. ) ;
#8191=( NAMED_UNIT ( * ) PLANE_ANGLE_UNIT ( ) SI_UNIT ( $, .RADIAN. ) );
#8210=LINE ( 'NONE', #936, #4161 ) ;
#8216=CARTESIAN_POINT ( 'NONE',  ( 0.000000000000000000, 0.000000000000000000, 42.00000000000000711 ) ) ;
#8222=CARTESIAN_POINT ( 'NONE',  ( 0.000000000000000000, 0.000000000000000000, 42.00000000000000711 ) ) ;
#8225=CARTESIAN_POINT ( 'NONE',  ( 0.000000000000000000, 0.000000000000000000, 120.0000000000000142 ) ) ;
#8227=EDGE_CURVE ( 'NONE', #5985, #2939, #8066, .T. ) ;
#8234=( GEOMETRIC_REPRESENTATION_CONTEXT ( 3 ) GLOBAL_UNCERTAINTY_ASSIGNED_CONTEXT ( ( #2388 ) ) GLOBAL_UNIT_ASSIGNED_CONTEXT ( ( #2179, #2272, #4221 ) ) REPRESENTATION_CONTEXT ( 'NONE', 'WORKASPACE' ) );
#8237=ORIENTED_EDGE ( 'NONE', *, *, #5913, .T. ) ;
#8250=VECTOR ( 'NONE', #1464, 1000.000000000000000 ) ;
#8279=ORIENTED_EDGE ( 'NONE', *, *, #1454, .F. ) ;
#8283=ADVANCED_FACE ( 'NONE', ( #7486 ), #4788, .F. ) ;
#8291=DIRECTION ( 'NONE',  ( 0.000000000000000000, -1.000000000000000000, 0.000000000000000000 ) ) ;
#8320=ORIENTED_EDGE ( 'NONE', *, *, #7553, .T. ) ;
#8330=FACE_OUTER_BOUND ( 'NONE', #7794, .T. ) ;
#8338=CARTESIAN_POINT ( 'NONE',  ( 0.000000000000000000, 0.000000000000000000, -14.56854249492377207 ) ) ;
#8343=ORIENTED_EDGE ( 'NONE', *, *, #5629, .T. ) ;
#8346=DIRECTION ( 'NONE',  ( 1.000000000000000000, 0.000000000000000000, 0.000000000000000000 ) ) ;
#8384=EDGE_LOOP ( 'NONE', ( #7996, #6240, #6738, #7835 ) ) ;
#8420=ORIENTED_EDGE ( 'NONE', *, *, #3748, .F. ) ;
#8442=ORIENTED_EDGE ( 'NONE', *, *, #7553, .F. ) ;
#8459=FACE_BOUND ( 'NONE', #4556, .T. ) ;
#8467=FACE_BOUND ( 'NONE', #5941, .T. ) ;
#8469=EDGE_CURVE ( 'NONE', #6087, #1828, #3521, .T. ) ;
#8498=EDGE_CURVE ( 'NONE', #6221, #8107, #1249, .T. ) ;
#8508=CARTESIAN_POINT ( 'NONE',  ( 0.000000000000000000, 0.000000000000000000, 120.0000000000000142 ) ) ;
#8511=CIRCLE ( 'NONE', #865, 20.00000000000000000 ) ;
#8513=CARTESIAN_POINT ( 'NONE',  ( 20.00000000000000000, 0.000000000000000000, 62.00000000000001421 ) ) ;
#8542=ADVANCED_FACE ( 'NONE', ( #7383 ), #8138, .T. ) ;
#8575=EDGE_LOOP ( 'NONE', ( #4876, #1217, #6489, #7301 ) ) ;
#8590=PLANE ( 'NONE',  #6058 ) ;
#8592=VERTEX_POINT ( 'NONE', #8050 ) ;
#8651=COLOUR_RGB('Sky Blue',0.24,0.69,0.87);
#8652=FILL_AREA_STYLE_COLOUR('',#8651);
#8653=FILL_AREA_STYLE('',(#8652));
#8654=SURFACE_STYLE_FILL_AREA(#8653);
#8655=SURFACE_SIDE_STYLE('',(#8654));
#8656=SURFACE_STYLE_USAGE(.BOTH.,#8655);
#8657=PRESENTATION_STYLE_ASSIGNMENT((#8656));
ENDSEC;
END-ISO-10303-21;
